ISO-10303-21;
HEADER;
/* Generated by software containing ST-Developer
 * from STEP Tools, Inc. (www.steptools.com) 
 */

FILE_DESCRIPTION(
/* description */ (''),
/* implementation_level */ '2;1');

FILE_NAME(
/* name */ '12_E-Clip_DIN_6799_-_5.step',
/* time_stamp */ '2026-10-26T03:55:20-07:00',
/* author */ (''),
/* organization */ (''),
/* preprocessor_version */ 'ST-DEVELOPER v20.2',
/* originating_system */ 'Autodesk Translation Framework v15.15.0.0',
/* authorisation */ '');

FILE_SCHEMA (('AUTOMOTIVE_DESIGN { 1 0 10303 214 3 1 1 }'));
ENDSEC;

DATA;
#10=MECHANICAL_DESIGN_GEOMETRIC_PRESENTATION_REPRESENTATION('',(#194),#45236);
#154=SHAPE_REPRESENTATION_RELATIONSHIP('SRR','None',#45333,#174);
#174=ADVANCED_BREP_SHAPE_REPRESENTATION('',(#214),#45235);
#194=STYLED_ITEM('',(#45470),#214);
#214=MANIFOLD_SOLID_BREP('Body1',#16536);
#1559=PLANE('',#18086);
#1560=PLANE('',#18090);
#1561=PLANE('',#18091);
#1562=PLANE('',#18092);
#1813=CYLINDRICAL_SURFACE('',#18083,5.5);
#1814=CYLINDRICAL_SURFACE('',#18087,2.5);
#2783=FACE_OUTER_BOUND('',#3880,.T.);
#2784=FACE_OUTER_BOUND('',#3881,.T.);
#2785=FACE_OUTER_BOUND('',#3882,.T.);
#2786=FACE_OUTER_BOUND('',#3883,.T.);
#2787=FACE_OUTER_BOUND('',#3884,.T.);
#2788=FACE_OUTER_BOUND('',#3885,.T.);
#3880=EDGE_LOOP('',(#15454,#15455,#15456,#15457));
#3881=EDGE_LOOP('',(#15458,#15459,#15460,#15461));
#3882=EDGE_LOOP('',(#15462,#15463,#15464,#15465));
#3883=EDGE_LOOP('',(#15466,#15467,#15468,#15469));
#3884=EDGE_LOOP('',(#15470,#15471,#15472,#15473));
#3885=EDGE_LOOP('',(#15474,#15475,#15476,#15477));
#5189=LINE('',#45142,#6500);
#5190=LINE('',#45145,#6501);
#5191=LINE('',#45148,#6502);
#5192=LINE('',#45150,#6503);
#5193=LINE('',#45151,#6504);
#5194=LINE('',#45157,#6505);
#5195=LINE('',#45159,#6506);
#5196=LINE('',#45160,#6507);
#6500=VECTOR('',#22080,10.);
#6501=VECTOR('',#22083,10.);
#6502=VECTOR('',#22086,10.);
#6503=VECTOR('',#22087,10.);
#6504=VECTOR('',#22088,10.);
#6505=VECTOR('',#22095,10.);
#6506=VECTOR('',#22098,10.);
#6507=VECTOR('',#22099,10.);
#6959=CIRCLE('',#18084,5.5);
#6960=CIRCLE('',#18085,5.5);
#6961=CIRCLE('',#18088,2.5);
#6962=CIRCLE('',#18089,2.5);
#8456=VERTEX_POINT('',#45138);
#8457=VERTEX_POINT('',#45139);
#8458=VERTEX_POINT('',#45141);
#8459=VERTEX_POINT('',#45143);
#8460=VERTEX_POINT('',#45147);
#8461=VERTEX_POINT('',#45149);
#8462=VERTEX_POINT('',#45153);
#8463=VERTEX_POINT('',#45155);
#10790=EDGE_CURVE('',#8456,#8457,#6959,.T.);
#10791=EDGE_CURVE('',#8457,#8458,#5189,.T.);
#10792=EDGE_CURVE('',#8459,#8458,#6960,.T.);
#10793=EDGE_CURVE('',#8456,#8459,#5190,.T.);
#10794=EDGE_CURVE('',#8456,#8460,#5191,.T.);
#10795=EDGE_CURVE('',#8461,#8459,#5192,.T.);
#10796=EDGE_CURVE('',#8460,#8461,#5193,.T.);
#10797=EDGE_CURVE('',#8460,#8462,#6961,.T.);
#10798=EDGE_CURVE('',#8463,#8461,#6962,.T.);
#10799=EDGE_CURVE('',#8462,#8463,#5194,.T.);
#10800=EDGE_CURVE('',#8457,#8462,#5195,.T.);
#10801=EDGE_CURVE('',#8458,#8463,#5196,.T.);
#15454=ORIENTED_EDGE('',*,*,#10790,.T.);
#15455=ORIENTED_EDGE('',*,*,#10791,.T.);
#15456=ORIENTED_EDGE('',*,*,#10792,.F.);
#15457=ORIENTED_EDGE('',*,*,#10793,.F.);
#15458=ORIENTED_EDGE('',*,*,#10794,.F.);
#15459=ORIENTED_EDGE('',*,*,#10793,.T.);
#15460=ORIENTED_EDGE('',*,*,#10795,.F.);
#15461=ORIENTED_EDGE('',*,*,#10796,.F.);
#15462=ORIENTED_EDGE('',*,*,#10797,.F.);
#15463=ORIENTED_EDGE('',*,*,#10796,.T.);
#15464=ORIENTED_EDGE('',*,*,#10798,.F.);
#15465=ORIENTED_EDGE('',*,*,#10799,.F.);
#15466=ORIENTED_EDGE('',*,*,#10800,.T.);
#15467=ORIENTED_EDGE('',*,*,#10799,.T.);
#15468=ORIENTED_EDGE('',*,*,#10801,.F.);
#15469=ORIENTED_EDGE('',*,*,#10791,.F.);
#15470=ORIENTED_EDGE('',*,*,#10801,.T.);
#15471=ORIENTED_EDGE('',*,*,#10798,.T.);
#15472=ORIENTED_EDGE('',*,*,#10795,.T.);
#15473=ORIENTED_EDGE('',*,*,#10792,.T.);
#15474=ORIENTED_EDGE('',*,*,#10800,.F.);
#15475=ORIENTED_EDGE('',*,*,#10790,.F.);
#15476=ORIENTED_EDGE('',*,*,#10794,.T.);
#15477=ORIENTED_EDGE('',*,*,#10797,.T.);
#16511=ADVANCED_FACE('',(#2783),#1813,.T.);
#16512=ADVANCED_FACE('',(#2784),#1559,.T.);
#16513=ADVANCED_FACE('',(#2785),#1814,.F.);
#16514=ADVANCED_FACE('',(#2786),#1560,.T.);
#16515=ADVANCED_FACE('',(#2787),#1561,.T.);
#16516=ADVANCED_FACE('',(#2788),#1562,.F.);
#16536=CLOSED_SHELL('',(#16511,#16512,#16513,#16514,#16515,#16516));
#18082=AXIS2_PLACEMENT_3D('',#45136,#22074,#22075);
#18083=AXIS2_PLACEMENT_3D('',#45137,#22076,#22077);
#18084=AXIS2_PLACEMENT_3D('',#45140,#22078,#22079);
#18085=AXIS2_PLACEMENT_3D('',#45144,#22081,#22082);
#18086=AXIS2_PLACEMENT_3D('',#45146,#22084,#22085);
#18087=AXIS2_PLACEMENT_3D('',#45152,#22089,#22090);
#18088=AXIS2_PLACEMENT_3D('',#45154,#22091,#22092);
#18089=AXIS2_PLACEMENT_3D('',#45156,#22093,#22094);
#18090=AXIS2_PLACEMENT_3D('',#45158,#22096,#22097);
#18091=AXIS2_PLACEMENT_3D('',#45161,#22100,#22101);
#18092=AXIS2_PLACEMENT_3D('',#45162,#22102,#22103);
#22074=DIRECTION('axis',(0.,0.,1.));
#22075=DIRECTION('refdir',(1.,0.,0.));
#22076=DIRECTION('center_axis',(1.,0.,0.));
#22077=DIRECTION('ref_axis',(0.,-8.07434927000114E-16,-1.));
#22078=DIRECTION('center_axis',(1.,0.,0.));
#22079=DIRECTION('ref_axis',(0.,-0.418181818181818,0.908363345221586));
#22080=DIRECTION('',(1.,0.,0.));
#22081=DIRECTION('center_axis',(1.,0.,0.));
#22082=DIRECTION('ref_axis',(0.,-0.418181818181818,0.908363345221586));
#22083=DIRECTION('',(1.,0.,0.));
#22084=DIRECTION('center_axis',(0.,1.,0.));
#22085=DIRECTION('ref_axis',(0.,0.,1.));
#22086=DIRECTION('',(0.,0.,-1.));
#22087=DIRECTION('',(0.,0.,1.));
#22088=DIRECTION('',(1.,0.,0.));
#22089=DIRECTION('center_axis',(1.,0.,0.));
#22090=DIRECTION('ref_axis',(0.,-1.11022302462516E-16,-1.));
#22091=DIRECTION('center_axis',(1.,0.,0.));
#22092=DIRECTION('ref_axis',(0.,-0.92,0.391918358845309));
#22093=DIRECTION('center_axis',(-1.,0.,0.));
#22094=DIRECTION('ref_axis',(0.,-0.92,0.391918358845309));
#22095=DIRECTION('',(1.,0.,0.));
#22096=DIRECTION('center_axis',(0.,-1.,0.));
#22097=DIRECTION('ref_axis',(0.,0.,-1.));
#22098=DIRECTION('',(0.,0.,-1.));
#22099=DIRECTION('',(0.,0.,-1.));
#22100=DIRECTION('center_axis',(1.,0.,0.));
#22101=DIRECTION('ref_axis',(0.,0.,-1.));
#22102=DIRECTION('center_axis',(1.,0.,0.));
#22103=DIRECTION('ref_axis',(0.,0.,-1.));
#45136=CARTESIAN_POINT('',(0.,0.,0.));
#45137=CARTESIAN_POINT('Origin',(0.,-2.63677968348475E-15,-2.77555756156289E-16));
#45138=CARTESIAN_POINT('',(0.,-2.3,4.99599839871872));
#45139=CARTESIAN_POINT('',(0.,2.3,4.99599839871872));
#45140=CARTESIAN_POINT('Origin',(0.,-2.63677968348475E-15,-2.77555756156289E-16));
#45141=CARTESIAN_POINT('',(0.7,2.3,4.99599839871872));
#45142=CARTESIAN_POINT('',(0.,2.3,4.99599839871872));
#45143=CARTESIAN_POINT('',(0.7,-2.3,4.99599839871872));
#45144=CARTESIAN_POINT('Origin',(0.7,-2.63677968348475E-15,-2.77555756156289E-16));
#45145=CARTESIAN_POINT('',(0.,-2.3,4.99599839871872));
#45146=CARTESIAN_POINT('Origin',(0.,-2.3,0.979795897113271));
#45147=CARTESIAN_POINT('',(0.,-2.3,0.979795897113271));
#45148=CARTESIAN_POINT('',(0.,-2.3,4.99599839871872));
#45149=CARTESIAN_POINT('',(0.7,-2.3,0.979795897113271));
#45150=CARTESIAN_POINT('',(0.7,-2.3,4.99599839871872));
#45151=CARTESIAN_POINT('',(0.,-2.3,0.979795897113271));
#45152=CARTESIAN_POINT('Origin',(0.,0.,-1.38777878078145E-16));
#45153=CARTESIAN_POINT('',(0.,2.3,0.979795897113271));
#45154=CARTESIAN_POINT('Origin',(0.,0.,-1.38777878078145E-16));
#45155=CARTESIAN_POINT('',(0.7,2.3,0.979795897113271));
#45156=CARTESIAN_POINT('Origin',(0.7,0.,-1.38777878078145E-16));
#45157=CARTESIAN_POINT('',(0.,2.3,0.979795897113271));
#45158=CARTESIAN_POINT('Origin',(0.,2.3,4.99599839871872));
#45159=CARTESIAN_POINT('',(0.,2.3,4.99599839871872));
#45160=CARTESIAN_POINT('',(0.7,2.3,4.99599839871872));
#45161=CARTESIAN_POINT('Origin',(0.7,-2.22044604925031E-15,-0.25200080064064));
#45162=CARTESIAN_POINT('Origin',(0.,-2.22044604925031E-15,-0.25200080064064));
#45213=UNCERTAINTY_MEASURE_WITH_UNIT(LENGTH_MEASURE(0.01),#45237,
'DISTANCE_ACCURACY_VALUE',
'Maximum model space distance between geometric entities at asserted c
onnectivities');
#45214=UNCERTAINTY_MEASURE_WITH_UNIT(LENGTH_MEASURE(0.01),#45237,
'DISTANCE_ACCURACY_VALUE',
'Maximum model space distance between geometric entities at asserted c
onnectivities');
#45235=(
GEOMETRIC_REPRESENTATION_CONTEXT(3)
GLOBAL_UNCERTAINTY_ASSIGNED_CONTEXT((#45213))
GLOBAL_UNIT_ASSIGNED_CONTEXT((#45237,#45239,#45240))
REPRESENTATION_CONTEXT('','3D')
);
#45236=(
GEOMETRIC_REPRESENTATION_CONTEXT(3)
GLOBAL_UNCERTAINTY_ASSIGNED_CONTEXT((#45214))
GLOBAL_UNIT_ASSIGNED_CONTEXT((#45237,#45239,#45240))
REPRESENTATION_CONTEXT('','3D')
);
#45237=(
LENGTH_UNIT()
NAMED_UNIT(*)
SI_UNIT(.MILLI.,.METRE.)
);
#45239=(
NAMED_UNIT(*)
PLANE_ANGLE_UNIT()
SI_UNIT($,.RADIAN.)
);
#45240=(
NAMED_UNIT(*)
SI_UNIT($,.STERADIAN.)
SOLID_ANGLE_UNIT()
);
#45261=SHAPE_DEFINITION_REPRESENTATION(#45282,#45333);
#45282=PRODUCT_DEFINITION_SHAPE('',$,#45355);
#45333=SHAPE_REPRESENTATION('',(#18082),#45235);
#45334=PRODUCT_DEFINITION_CONTEXT('part definition',#45399,'design');
#45355=PRODUCT_DEFINITION('2026-10-25-23-38-20-982',
'12_E-Clip_DIN_6799_-_5',#45376,#45334);
#45376=PRODUCT_DEFINITION_FORMATION('',$,#45421);
#45399=APPLICATION_CONTEXT(
'Core Data for Automotive Mechanical Design Process');
#45400=PRODUCT_CONTEXT('part definition',#45399,'mechanical');
#45421=PRODUCT('2026-10-25-23-38-20-982','12_E-Clip_DIN_6799_-_5',$,(#45400));
#45464=COLOUR_RGB('Light Blue',0.38,0.62,0.78);
#45465=FILL_AREA_STYLE_COLOUR('',#45464);
#45466=FILL_AREA_STYLE('',(#45465));
#45467=SURFACE_STYLE_FILL_AREA(#45466);
#45468=SURFACE_SIDE_STYLE('',(#45467));
#45469=SURFACE_STYLE_USAGE(.BOTH.,#45468);
#45470=PRESENTATION_STYLE_ASSIGNMENT((#45469));
ENDSEC;
END-ISO-10303-21;
